ISO-10303-21;
HEADER;
/* Generated by software containing ST-Developer
 * from STEP Tools, Inc. (www.steptools.com) 
 */

FILE_DESCRIPTION(
/* description */ ('PAT-091'),
/* implementation_level */ '2;1');

FILE_NAME(
/* name */ 'Axle end keeper (6).step',
/* time_stamp */ '2026-10-27T15:34:44-07:00',
/* author */ (''),
/* organization */ (''),
/* preprocessor_version */ 'ST-DEVELOPER v20.2',
/* originating_system */ 'Autodesk Translation Framework v15.17.0.0',
/* authorisation */ '');

FILE_SCHEMA (('AUTOMOTIVE_DESIGN { 1 0 10303 214 3 1 1 }'));
ENDSEC;

DATA;
#10=MECHANICAL_DESIGN_GEOMETRIC_PRESENTATION_REPRESENTATION('',(#1018),#25100);
#798=SHAPE_REPRESENTATION_RELATIONSHIP('SRR','None',#25562,#908);
#908=ADVANCED_BREP_SHAPE_REPRESENTATION('',(#1140),#25032);
#1018=STYLED_ITEM('',(#26191),#1140);
#1140=MANIFOLD_SOLID_BREP('Body1',#13297);
#1460=FACE_BOUND('',#3517,.T.);
#1461=FACE_BOUND('',#3519,.T.);
#1857=PLANE('',#15371);
#1858=PLANE('',#15372);
#2451=FACE_OUTER_BOUND('',#3514,.T.);
#2452=FACE_OUTER_BOUND('',#3515,.T.);
#2453=FACE_OUTER_BOUND('',#3516,.T.);
#2454=FACE_OUTER_BOUND('',#3518,.T.);
#3514=EDGE_LOOP('',(#10560,#10561,#10562,#10563));
#3515=EDGE_LOOP('',(#10564,#10565,#10566,#10567));
#3516=EDGE_LOOP('',(#10568));
#3517=EDGE_LOOP('',(#10569));
#3518=EDGE_LOOP('',(#10570));
#3519=EDGE_LOOP('',(#10571));
#4575=LINE('',#22792,#5315);
#4576=LINE('',#22798,#5316);
#5315=VECTOR('',#18483,0.225000000000001);
#5316=VECTOR('',#18490,1.);
#5943=CIRCLE('',#15366,0.225000000000001);
#5944=CIRCLE('',#15367,0.225000000000001);
#5945=CIRCLE('',#15369,1.);
#5946=CIRCLE('',#15370,1.);
#6910=VERTEX_POINT('',#22789);
#6911=VERTEX_POINT('',#22791);
#6912=VERTEX_POINT('',#22795);
#6913=VERTEX_POINT('',#22797);
#8215=EDGE_CURVE('',#6910,#6910,#5943,.T.);
#8216=EDGE_CURVE('',#6910,#6911,#4575,.T.);
#8217=EDGE_CURVE('',#6911,#6911,#5944,.T.);
#8218=EDGE_CURVE('',#6912,#6912,#5945,.T.);
#8219=EDGE_CURVE('',#6912,#6913,#4576,.T.);
#8220=EDGE_CURVE('',#6913,#6913,#5946,.T.);
#10560=ORIENTED_EDGE('',*,*,#8215,.F.);
#10561=ORIENTED_EDGE('',*,*,#8216,.T.);
#10562=ORIENTED_EDGE('',*,*,#8217,.T.);
#10563=ORIENTED_EDGE('',*,*,#8216,.F.);
#10564=ORIENTED_EDGE('',*,*,#8218,.F.);
#10565=ORIENTED_EDGE('',*,*,#8219,.T.);
#10566=ORIENTED_EDGE('',*,*,#8220,.T.);
#10567=ORIENTED_EDGE('',*,*,#8219,.F.);
#10568=ORIENTED_EDGE('',*,*,#8218,.T.);
#10569=ORIENTED_EDGE('',*,*,#8215,.T.);
#10570=ORIENTED_EDGE('',*,*,#8220,.F.);
#10571=ORIENTED_EDGE('',*,*,#8217,.F.);
#12238=CYLINDRICAL_SURFACE('',#15365,0.225000000000001);
#12239=CYLINDRICAL_SURFACE('',#15368,1.);
#12818=ADVANCED_FACE('',(#2451),#12238,.F.);
#12819=ADVANCED_FACE('',(#2452),#12239,.T.);
#12820=ADVANCED_FACE('',(#2453,#1460),#1857,.T.);
#12821=ADVANCED_FACE('',(#2454,#1461),#1858,.F.);
#13297=CLOSED_SHELL('',(#12818,#12819,#12820,#12821));
#15364=AXIS2_PLACEMENT_3D('',#22787,#18477,#18478);
#15365=AXIS2_PLACEMENT_3D('',#22788,#18479,#18480);
#15366=AXIS2_PLACEMENT_3D('',#22790,#18481,#18482);
#15367=AXIS2_PLACEMENT_3D('',#22793,#18484,#18485);
#15368=AXIS2_PLACEMENT_3D('',#22794,#18486,#18487);
#15369=AXIS2_PLACEMENT_3D('',#22796,#18488,#18489);
#15370=AXIS2_PLACEMENT_3D('',#22799,#18491,#18492);
#15371=AXIS2_PLACEMENT_3D('',#22800,#18493,#18494);
#15372=AXIS2_PLACEMENT_3D('',#22801,#18495,#18496);
#18477=DIRECTION('axis',(0.,0.,1.));
#18478=DIRECTION('refdir',(1.,0.,0.));
#18479=DIRECTION('center_axis',(0.,1.,0.));
#18480=DIRECTION('ref_axis',(1.,0.,0.));
#18481=DIRECTION('center_axis',(0.,-1.,0.));
#18482=DIRECTION('ref_axis',(1.,0.,0.));
#18483=DIRECTION('',(0.,-1.,0.));
#18484=DIRECTION('center_axis',(0.,-1.,0.));
#18485=DIRECTION('ref_axis',(1.,0.,0.));
#18486=DIRECTION('center_axis',(0.,1.,0.));
#18487=DIRECTION('ref_axis',(1.,0.,0.));
#18488=DIRECTION('center_axis',(0.,1.,0.));
#18489=DIRECTION('ref_axis',(1.,0.,0.));
#18490=DIRECTION('',(0.,-1.,0.));
#18491=DIRECTION('center_axis',(0.,1.,0.));
#18492=DIRECTION('ref_axis',(1.,0.,0.));
#18493=DIRECTION('center_axis',(0.,1.,0.));
#18494=DIRECTION('ref_axis',(1.,0.,0.));
#18495=DIRECTION('center_axis',(0.,1.,0.));
#18496=DIRECTION('ref_axis',(1.,0.,0.));
#22787=CARTESIAN_POINT('',(0.,0.,0.));
#22788=CARTESIAN_POINT('Origin',(38.7298334620742,-7.7,13.));
#22789=CARTESIAN_POINT('',(38.5048334620742,-7.5,13.));
#22790=CARTESIAN_POINT('Origin',(38.7298334620742,-7.5,13.));
#22791=CARTESIAN_POINT('',(38.5048334620742,-7.7,13.));
#22792=CARTESIAN_POINT('',(38.5048334620742,-7.7,13.));
#22793=CARTESIAN_POINT('Origin',(38.7298334620742,-7.7,13.));
#22794=CARTESIAN_POINT('Origin',(38.7298334620742,-7.7,13.));
#22795=CARTESIAN_POINT('',(37.7298334620742,-7.5,13.));
#22796=CARTESIAN_POINT('Origin',(38.7298334620742,-7.5,13.));
#22797=CARTESIAN_POINT('',(37.7298334620742,-7.7,13.));
#22798=CARTESIAN_POINT('',(37.7298334620742,-7.7,13.));
#22799=CARTESIAN_POINT('Origin',(38.7298334620742,-7.7,13.));
#22800=CARTESIAN_POINT('Origin',(38.7298334620742,-7.5,13.));
#22801=CARTESIAN_POINT('Origin',(38.7298334620742,-7.7,13.));
#24911=UNCERTAINTY_MEASURE_WITH_UNIT(LENGTH_MEASURE(0.001),#25101,
'DISTANCE_ACCURACY_VALUE',
'Maximum model space distance between geometric entities at asserted c
onnectivities');
#24979=UNCERTAINTY_MEASURE_WITH_UNIT(LENGTH_MEASURE(0.001),#25101,
'DISTANCE_ACCURACY_VALUE',
'Maximum model space distance between geometric entities at asserted c
onnectivities');
#25032=(
GEOMETRIC_REPRESENTATION_CONTEXT(3)
GLOBAL_UNCERTAINTY_ASSIGNED_CONTEXT((#24911))
GLOBAL_UNIT_ASSIGNED_CONTEXT((#25101,#25103,#25104))
REPRESENTATION_CONTEXT('','3D')
);
#25100=(
GEOMETRIC_REPRESENTATION_CONTEXT(3)
GLOBAL_UNCERTAINTY_ASSIGNED_CONTEXT((#24979))
GLOBAL_UNIT_ASSIGNED_CONTEXT((#25101,#25103,#25104))
REPRESENTATION_CONTEXT('','3D')
);
#25101=(
LENGTH_UNIT()
NAMED_UNIT(*)
SI_UNIT(.CENTI.,.METRE.)
);
#25103=(
NAMED_UNIT(*)
PLANE_ANGLE_UNIT()
SI_UNIT($,.RADIAN.)
);
#25104=(
NAMED_UNIT(*)
SI_UNIT($,.STERADIAN.)
SOLID_ANGLE_UNIT()
);
#25157=SHAPE_DEFINITION_REPRESENTATION(#25277,#25562);
#25277=PRODUCT_DEFINITION_SHAPE('',$,#25683);
#25562=SHAPE_REPRESENTATION('',(#15364),#25032);
#25630=PRODUCT_DEFINITION_CONTEXT('part definition',#25992,'design');
#25683=PRODUCT_DEFINITION('Axle end keeper (6)','Axle end keeper (6)',#25803,
#25630);
#25803=PRODUCT_DEFINITION_FORMATION('',$,#26046);
#25992=APPLICATION_CONTEXT(
'Core Data for Automotive Mechanical Design Process');
#25993=PRODUCT_CONTEXT('part definition',#25992,'mechanical');
#26046=PRODUCT('Axle end keeper (6)','Axle end keeper (6)',
'Axle end keeper (6)',(#25993));
#26185=COLOUR_RGB('Grey',0.48,0.52,0.57);
#26186=FILL_AREA_STYLE_COLOUR('',#26185);
#26187=FILL_AREA_STYLE('',(#26186));
#26188=SURFACE_STYLE_FILL_AREA(#26187);
#26189=SURFACE_SIDE_STYLE('',(#26188));
#26190=SURFACE_STYLE_USAGE(.BOTH.,#26189);
#26191=PRESENTATION_STYLE_ASSIGNMENT((#26190));
ENDSEC;
END-ISO-10303-21;
